ISO-10303-21;
HEADER;
/* Generated by software containing ST-Developer
 * from STEP Tools, Inc. (www.steptools.com) 
 */

FILE_DESCRIPTION(
/* description */ (''),
/* implementation_level */ '2;1');

FILE_NAME(
/* name */ 'PO8.step',
/* time_stamp */ '2026-10-06T10:18:54-07:00',
/* author */ (''),
/* organization */ (''),
/* preprocessor_version */ 'ST-DEVELOPER v20.2',
/* originating_system */ 'Autodesk Translation Framework v15.15.0.0',
/* authorisation */ '');

FILE_SCHEMA (('AUTOMOTIVE_DESIGN { 1 0 10303 214 3 1 1 }'));
ENDSEC;

DATA;
#10=MECHANICAL_DESIGN_GEOMETRIC_PRESENTATION_REPRESENTATION('',(#86),#8445);
#68=SHAPE_REPRESENTATION_RELATIONSHIP('SRR','None',#8489,#77);
#77=ADVANCED_BREP_SHAPE_REPRESENTATION('',(#95),#8441);
#86=STYLED_ITEM('',(#8537),#95);
#95=MANIFOLD_SOLID_BREP('Body1',#4007);
#155=CYLINDRICAL_SURFACE('',#4415,1.25);
#156=CYLINDRICAL_SURFACE('',#4418,5.00000007450581);
#157=CYLINDRICAL_SURFACE('',#4422,0.999999999999998);
#158=CYLINDRICAL_SURFACE('',#4425,15.);
#159=CYLINDRICAL_SURFACE('',#4428,1.);
#361=FACE_BOUND('',#984,.T.);
#362=FACE_BOUND('',#986,.T.);
#488=CIRCLE('',#4416,1.25);
#489=CIRCLE('',#4417,1.25);
#490=CIRCLE('',#4419,5.00000007450581);
#491=CIRCLE('',#4420,5.00000007450581);
#492=CIRCLE('',#4423,0.999999999999998);
#493=CIRCLE('',#4424,0.999999999999998);
#494=CIRCLE('',#4426,15.);
#495=CIRCLE('',#4427,15.);
#496=CIRCLE('',#4429,1.);
#497=CIRCLE('',#4430,1.);
#717=FACE_OUTER_BOUND('',#976,.T.);
#718=FACE_OUTER_BOUND('',#977,.T.);
#719=FACE_OUTER_BOUND('',#978,.T.);
#720=FACE_OUTER_BOUND('',#979,.T.);
#721=FACE_OUTER_BOUND('',#980,.T.);
#722=FACE_OUTER_BOUND('',#981,.T.);
#723=FACE_OUTER_BOUND('',#982,.T.);
#724=FACE_OUTER_BOUND('',#983,.T.);
#725=FACE_OUTER_BOUND('',#985,.T.);
#976=EDGE_LOOP('',(#3473,#3474,#3475,#3476));
#977=EDGE_LOOP('',(#3477,#3478,#3479,#3480));
#978=EDGE_LOOP('',(#3481,#3482,#3483,#3484));
#979=EDGE_LOOP('',(#3485,#3486,#3487,#3488));
#980=EDGE_LOOP('',(#3489,#3490,#3491,#3492));
#981=EDGE_LOOP('',(#3493,#3494,#3495,#3496));
#982=EDGE_LOOP('',(#3497,#3498,#3499,#3500));
#983=EDGE_LOOP('',(#3501,#3502,#3503,#3504,#3505,#3506));
#984=EDGE_LOOP('',(#3507));
#985=EDGE_LOOP('',(#3508,#3509,#3510,#3511,#3512,#3513));
#986=EDGE_LOOP('',(#3514));
#1265=LINE('',#8218,#1554);
#1266=LINE('',#8225,#1555);
#1267=LINE('',#8228,#1556);
#1268=LINE('',#8231,#1557);
#1269=LINE('',#8233,#1558);
#1270=LINE('',#8234,#1559);
#1271=LINE('',#8240,#1560);
#1272=LINE('',#8246,#1561);
#1273=LINE('',#8252,#1562);
#1274=LINE('',#8254,#1563);
#1275=LINE('',#8255,#1564);
#1554=VECTOR('',#5362,1.25);
#1555=VECTOR('',#5369,10.);
#1556=VECTOR('',#5372,10.);
#1557=VECTOR('',#5375,10.);
#1558=VECTOR('',#5376,10.);
#1559=VECTOR('',#5377,10.);
#1560=VECTOR('',#5384,10.);
#1561=VECTOR('',#5391,10.);
#1562=VECTOR('',#5398,10.);
#1563=VECTOR('',#5401,10.);
#1564=VECTOR('',#5402,10.);
#1904=VERTEX_POINT('',#8215);
#1905=VERTEX_POINT('',#8217);
#1906=VERTEX_POINT('',#8221);
#1907=VERTEX_POINT('',#8222);
#1908=VERTEX_POINT('',#8224);
#1909=VERTEX_POINT('',#8226);
#1910=VERTEX_POINT('',#8230);
#1911=VERTEX_POINT('',#8232);
#1912=VERTEX_POINT('',#8236);
#1913=VERTEX_POINT('',#8238);
#1914=VERTEX_POINT('',#8242);
#1915=VERTEX_POINT('',#8244);
#1916=VERTEX_POINT('',#8248);
#1917=VERTEX_POINT('',#8250);
#2437=EDGE_CURVE('',#1904,#1904,#488,.T.);
#2438=EDGE_CURVE('',#1904,#1905,#1265,.T.);
#2439=EDGE_CURVE('',#1905,#1905,#489,.T.);
#2440=EDGE_CURVE('',#1906,#1907,#490,.T.);
#2441=EDGE_CURVE('',#1906,#1908,#1266,.T.);
#2442=EDGE_CURVE('',#1909,#1908,#491,.T.);
#2443=EDGE_CURVE('',#1907,#1909,#1267,.T.);
#2444=EDGE_CURVE('',#1907,#1910,#1268,.T.);
#2445=EDGE_CURVE('',#1911,#1909,#1269,.T.);
#2446=EDGE_CURVE('',#1910,#1911,#1270,.T.);
#2447=EDGE_CURVE('',#1912,#1910,#492,.T.);
#2448=EDGE_CURVE('',#1913,#1911,#493,.T.);
#2449=EDGE_CURVE('',#1912,#1913,#1271,.T.);
#2450=EDGE_CURVE('',#1914,#1912,#494,.T.);
#2451=EDGE_CURVE('',#1915,#1913,#495,.T.);
#2452=EDGE_CURVE('',#1914,#1915,#1272,.T.);
#2453=EDGE_CURVE('',#1916,#1914,#496,.T.);
#2454=EDGE_CURVE('',#1917,#1915,#497,.T.);
#2455=EDGE_CURVE('',#1916,#1917,#1273,.T.);
#2456=EDGE_CURVE('',#1906,#1916,#1274,.T.);
#2457=EDGE_CURVE('',#1908,#1917,#1275,.T.);
#3473=ORIENTED_EDGE('',*,*,#2437,.F.);
#3474=ORIENTED_EDGE('',*,*,#2438,.T.);
#3475=ORIENTED_EDGE('',*,*,#2439,.T.);
#3476=ORIENTED_EDGE('',*,*,#2438,.F.);
#3477=ORIENTED_EDGE('',*,*,#2440,.F.);
#3478=ORIENTED_EDGE('',*,*,#2441,.T.);
#3479=ORIENTED_EDGE('',*,*,#2442,.F.);
#3480=ORIENTED_EDGE('',*,*,#2443,.F.);
#3481=ORIENTED_EDGE('',*,*,#2444,.F.);
#3482=ORIENTED_EDGE('',*,*,#2443,.T.);
#3483=ORIENTED_EDGE('',*,*,#2445,.F.);
#3484=ORIENTED_EDGE('',*,*,#2446,.F.);
#3485=ORIENTED_EDGE('',*,*,#2447,.T.);
#3486=ORIENTED_EDGE('',*,*,#2446,.T.);
#3487=ORIENTED_EDGE('',*,*,#2448,.F.);
#3488=ORIENTED_EDGE('',*,*,#2449,.F.);
#3489=ORIENTED_EDGE('',*,*,#2450,.T.);
#3490=ORIENTED_EDGE('',*,*,#2449,.T.);
#3491=ORIENTED_EDGE('',*,*,#2451,.F.);
#3492=ORIENTED_EDGE('',*,*,#2452,.F.);
#3493=ORIENTED_EDGE('',*,*,#2453,.T.);
#3494=ORIENTED_EDGE('',*,*,#2452,.T.);
#3495=ORIENTED_EDGE('',*,*,#2454,.F.);
#3496=ORIENTED_EDGE('',*,*,#2455,.F.);
#3497=ORIENTED_EDGE('',*,*,#2456,.T.);
#3498=ORIENTED_EDGE('',*,*,#2455,.T.);
#3499=ORIENTED_EDGE('',*,*,#2457,.F.);
#3500=ORIENTED_EDGE('',*,*,#2441,.F.);
#3501=ORIENTED_EDGE('',*,*,#2457,.T.);
#3502=ORIENTED_EDGE('',*,*,#2454,.T.);
#3503=ORIENTED_EDGE('',*,*,#2451,.T.);
#3504=ORIENTED_EDGE('',*,*,#2448,.T.);
#3505=ORIENTED_EDGE('',*,*,#2445,.T.);
#3506=ORIENTED_EDGE('',*,*,#2442,.T.);
#3507=ORIENTED_EDGE('',*,*,#2437,.T.);
#3508=ORIENTED_EDGE('',*,*,#2456,.F.);
#3509=ORIENTED_EDGE('',*,*,#2440,.T.);
#3510=ORIENTED_EDGE('',*,*,#2444,.T.);
#3511=ORIENTED_EDGE('',*,*,#2447,.F.);
#3512=ORIENTED_EDGE('',*,*,#2450,.F.);
#3513=ORIENTED_EDGE('',*,*,#2453,.F.);
#3514=ORIENTED_EDGE('',*,*,#2439,.F.);
#3739=PLANE('',#4421);
#3740=PLANE('',#4431);
#3741=PLANE('',#4432);
#3742=PLANE('',#4433);
#3958=ADVANCED_FACE('',(#717),#155,.F.);
#3959=ADVANCED_FACE('',(#718),#156,.F.);
#3960=ADVANCED_FACE('',(#719),#3739,.T.);
#3961=ADVANCED_FACE('',(#720),#157,.T.);
#3962=ADVANCED_FACE('',(#721),#158,.T.);
#3963=ADVANCED_FACE('',(#722),#159,.T.);
#3964=ADVANCED_FACE('',(#723),#3740,.T.);
#3965=ADVANCED_FACE('',(#724,#361),#3741,.T.);
#3966=ADVANCED_FACE('',(#725,#362),#3742,.F.);
#4007=CLOSED_SHELL('',(#3958,#3959,#3960,#3961,#3962,#3963,#3964,#3965,
#3966));
#4414=AXIS2_PLACEMENT_3D('',#8213,#5356,#5357);
#4415=AXIS2_PLACEMENT_3D('',#8214,#5358,#5359);
#4416=AXIS2_PLACEMENT_3D('',#8216,#5360,#5361);
#4417=AXIS2_PLACEMENT_3D('',#8219,#5363,#5364);
#4418=AXIS2_PLACEMENT_3D('',#8220,#5365,#5366);
#4419=AXIS2_PLACEMENT_3D('',#8223,#5367,#5368);
#4420=AXIS2_PLACEMENT_3D('',#8227,#5370,#5371);
#4421=AXIS2_PLACEMENT_3D('',#8229,#5373,#5374);
#4422=AXIS2_PLACEMENT_3D('',#8235,#5378,#5379);
#4423=AXIS2_PLACEMENT_3D('',#8237,#5380,#5381);
#4424=AXIS2_PLACEMENT_3D('',#8239,#5382,#5383);
#4425=AXIS2_PLACEMENT_3D('',#8241,#5385,#5386);
#4426=AXIS2_PLACEMENT_3D('',#8243,#5387,#5388);
#4427=AXIS2_PLACEMENT_3D('',#8245,#5389,#5390);
#4428=AXIS2_PLACEMENT_3D('',#8247,#5392,#5393);
#4429=AXIS2_PLACEMENT_3D('',#8249,#5394,#5395);
#4430=AXIS2_PLACEMENT_3D('',#8251,#5396,#5397);
#4431=AXIS2_PLACEMENT_3D('',#8253,#5399,#5400);
#4432=AXIS2_PLACEMENT_3D('',#8256,#5403,#5404);
#4433=AXIS2_PLACEMENT_3D('',#8257,#5405,#5406);
#5356=DIRECTION('axis',(0.,0.,1.));
#5357=DIRECTION('refdir',(1.,0.,0.));
#5358=DIRECTION('center_axis',(0.,0.,1.));
#5359=DIRECTION('ref_axis',(1.,0.,0.));
#5360=DIRECTION('center_axis',(0.,0.,-1.));
#5361=DIRECTION('ref_axis',(1.,0.,0.));
#5362=DIRECTION('',(0.,0.,-1.));
#5363=DIRECTION('center_axis',(0.,0.,-1.));
#5364=DIRECTION('ref_axis',(1.,0.,0.));
#5365=DIRECTION('center_axis',(0.,0.,1.));
#5366=DIRECTION('ref_axis',(0.,1.,0.));
#5367=DIRECTION('center_axis',(0.,0.,1.));
#5368=DIRECTION('ref_axis',(0.,1.,0.));
#5369=DIRECTION('',(0.,0.,1.));
#5370=DIRECTION('center_axis',(0.,0.,-1.));
#5371=DIRECTION('ref_axis',(0.,1.,0.));
#5372=DIRECTION('',(0.,0.,1.));
#5373=DIRECTION('center_axis',(0.,1.,0.));
#5374=DIRECTION('ref_axis',(-1.,0.,0.));
#5375=DIRECTION('',(1.,0.,0.));
#5376=DIRECTION('',(-1.,0.,0.));
#5377=DIRECTION('',(0.,0.,1.));
#5378=DIRECTION('center_axis',(0.,0.,1.));
#5379=DIRECTION('ref_axis',(0.90350790038088,-0.428571433893271,0.));
#5380=DIRECTION('center_axis',(0.,0.,1.));
#5381=DIRECTION('ref_axis',(0.90350790038088,-0.428571433893271,0.));
#5382=DIRECTION('center_axis',(0.,0.,1.));
#5383=DIRECTION('ref_axis',(0.90350790038088,-0.428571433893271,0.));
#5384=DIRECTION('',(0.,0.,1.));
#5385=DIRECTION('center_axis',(0.,0.,1.));
#5386=DIRECTION('ref_axis',(-1.,-2.96059473233375E-16,0.));
#5387=DIRECTION('center_axis',(0.,0.,1.));
#5388=DIRECTION('ref_axis',(0.903507900380879,0.428571433893272,0.));
#5389=DIRECTION('center_axis',(0.,0.,1.));
#5390=DIRECTION('ref_axis',(0.903507900380879,0.428571433893272,0.));
#5391=DIRECTION('',(0.,0.,1.));
#5392=DIRECTION('center_axis',(0.,0.,1.));
#5393=DIRECTION('ref_axis',(0.,-1.,0.));
#5394=DIRECTION('center_axis',(0.,0.,1.));
#5395=DIRECTION('ref_axis',(0.,-1.,0.));
#5396=DIRECTION('center_axis',(0.,0.,1.));
#5397=DIRECTION('ref_axis',(0.,-1.,0.));
#5398=DIRECTION('',(0.,0.,1.));
#5399=DIRECTION('center_axis',(0.,-1.,0.));
#5400=DIRECTION('ref_axis',(1.,0.,0.));
#5401=DIRECTION('',(1.,0.,0.));
#5402=DIRECTION('',(1.,0.,0.));
#5403=DIRECTION('center_axis',(0.,0.,1.));
#5404=DIRECTION('ref_axis',(1.,0.,0.));
#5405=DIRECTION('center_axis',(0.,0.,1.));
#5406=DIRECTION('ref_axis',(1.,0.,0.));
#8213=CARTESIAN_POINT('',(0.,0.,0.));
#8214=CARTESIAN_POINT('Origin',(0.,12.5,0.));
#8215=CARTESIAN_POINT('',(-1.25,12.5,3.3));
#8216=CARTESIAN_POINT('Origin',(0.,12.5,3.3));
#8217=CARTESIAN_POINT('',(-1.25,12.5,0.));
#8218=CARTESIAN_POINT('',(-1.25,12.5,0.));
#8219=CARTESIAN_POINT('Origin',(0.,12.5,0.));
#8220=CARTESIAN_POINT('Origin',(0.,0.,0.));
#8221=CARTESIAN_POINT('',(0.,5.00000007450581,0.));
#8222=CARTESIAN_POINT('',(-6.12323408698006E-16,-5.00000007450581,0.));
#8223=CARTESIAN_POINT('Origin',(0.,0.,0.));
#8224=CARTESIAN_POINT('',(0.,5.00000007450581,3.3));
#8225=CARTESIAN_POINT('',(0.,5.00000007450581,0.));
#8226=CARTESIAN_POINT('',(-5.55111512312578E-16,-5.00000007450581,3.3));
#8227=CARTESIAN_POINT('Origin',(0.,0.,3.3));
#8228=CARTESIAN_POINT('',(-6.12323408698006E-16,-5.00000007450581,0.));
#8229=CARTESIAN_POINT('Origin',(12.6491106053323,-5.00000007450581,0.));
#8230=CARTESIAN_POINT('',(12.6491106053323,-5.00000007450581,0.));
#8231=CARTESIAN_POINT('',(0.,-5.00000007450581,0.));
#8232=CARTESIAN_POINT('',(12.6491106053323,-5.00000007450581,3.3));
#8233=CARTESIAN_POINT('',(0.,-5.00000007450581,3.3));
#8234=CARTESIAN_POINT('',(12.6491106053323,-5.00000007450581,0.));
#8235=CARTESIAN_POINT('Origin',(12.6491106053323,-6.0000000745058,0.));
#8236=CARTESIAN_POINT('',(13.5526185057132,-6.42857150839907,0.));
#8237=CARTESIAN_POINT('Origin',(12.6491106053323,-6.0000000745058,0.));
#8238=CARTESIAN_POINT('',(13.5526185057132,-6.42857150839907,3.3));
#8239=CARTESIAN_POINT('Origin',(12.6491106053323,-6.0000000745058,3.3));
#8240=CARTESIAN_POINT('',(13.5526185057132,-6.42857150839907,0.));
#8241=CARTESIAN_POINT('Origin',(0.,0.,0.));
#8242=CARTESIAN_POINT('',(13.5526185057132,6.42857150839908,0.));
#8243=CARTESIAN_POINT('Origin',(0.,0.,0.));
#8244=CARTESIAN_POINT('',(13.5526185057132,6.42857150839908,3.3));
#8245=CARTESIAN_POINT('Origin',(0.,0.,3.3));
#8246=CARTESIAN_POINT('',(13.5526185057132,6.42857150839908,0.));
#8247=CARTESIAN_POINT('Origin',(12.6491106053323,6.00000007450581,0.));
#8248=CARTESIAN_POINT('',(12.6491106053323,5.00000007450581,0.));
#8249=CARTESIAN_POINT('Origin',(12.6491106053323,6.00000007450581,0.));
#8250=CARTESIAN_POINT('',(12.6491106053323,5.00000007450581,3.3));
#8251=CARTESIAN_POINT('Origin',(12.6491106053323,6.00000007450581,3.3));
#8252=CARTESIAN_POINT('',(12.6491106053323,5.00000007450581,0.));
#8253=CARTESIAN_POINT('Origin',(0.,5.00000007450581,0.));
#8254=CARTESIAN_POINT('',(0.,5.00000007450581,0.));
#8255=CARTESIAN_POINT('',(0.,5.00000007450581,3.3));
#8256=CARTESIAN_POINT('Origin',(-0.675444697333845,0.,3.3));
#8257=CARTESIAN_POINT('Origin',(-0.675444697333845,0.,0.));
#8430=UNCERTAINTY_MEASURE_WITH_UNIT(LENGTH_MEASURE(0.01),#8446,
'DISTANCE_ACCURACY_VALUE',
'Maximum model space distance between geometric entities at asserted c
onnectivities');
#8434=UNCERTAINTY_MEASURE_WITH_UNIT(LENGTH_MEASURE(0.01),#8446,
'DISTANCE_ACCURACY_VALUE',
'Maximum model space distance between geometric entities at asserted c
onnectivities');
#8441=(
GEOMETRIC_REPRESENTATION_CONTEXT(3)
GLOBAL_UNCERTAINTY_ASSIGNED_CONTEXT((#8430))
GLOBAL_UNIT_ASSIGNED_CONTEXT((#8446,#8448,#8449))
REPRESENTATION_CONTEXT('','3D')
);
#8445=(
GEOMETRIC_REPRESENTATION_CONTEXT(3)
GLOBAL_UNCERTAINTY_ASSIGNED_CONTEXT((#8434))
GLOBAL_UNIT_ASSIGNED_CONTEXT((#8446,#8448,#8449))
REPRESENTATION_CONTEXT('','3D')
);
#8446=(
LENGTH_UNIT()
NAMED_UNIT(*)
SI_UNIT(.MILLI.,.METRE.)
);
#8448=(
NAMED_UNIT(*)
PLANE_ANGLE_UNIT()
SI_UNIT($,.RADIAN.)
);
#8449=(
NAMED_UNIT(*)
SI_UNIT($,.STERADIAN.)
SOLID_ANGLE_UNIT()
);
#8456=SHAPE_DEFINITION_REPRESENTATION(#8466,#8489);
#8466=PRODUCT_DEFINITION_SHAPE('',$,#8500);
#8489=SHAPE_REPRESENTATION('',(#4414),#8441);
#8493=PRODUCT_DEFINITION_CONTEXT('part definition',#8525,'design');
#8500=PRODUCT_DEFINITION('2026-10-05-11-51-25-783','PO8',#8510,#8493);
#8510=PRODUCT_DEFINITION_FORMATION('',$,#8533);
#8525=APPLICATION_CONTEXT(
'Core Data for Automotive Mechanical Design Process');
#8526=PRODUCT_CONTEXT('part definition',#8525,'mechanical');
#8533=PRODUCT('2026-10-05-11-51-25-783','PO8',$,(#8526));
#8537=PRESENTATION_STYLE_ASSIGNMENT((#8538));
#8538=SURFACE_STYLE_USAGE(.BOTH.,#8539);
#8539=SURFACE_SIDE_STYLE('',(#8540));
#8540=SURFACE_STYLE_FILL_AREA(#8541);
#8541=FILL_AREA_STYLE('Steel - Satin',(#8542));
#8542=FILL_AREA_STYLE_COLOUR('Steel - Satin',#8543);
#8543=COLOUR_RGB('Steel - Satin', 0.09019608, 0.27058824, 0.51372549);
ENDSEC;
END-ISO-10303-21;
